ISO-10303-21;
HEADER;
/* Generated by software containing ST-Developer
 * from STEP Tools, Inc. (www.steptools.com) 
 */

FILE_DESCRIPTION(
/* description */ (''),
/* implementation_level */ '2;1');

FILE_NAME(
/* name */ 'Blade_07.step',
/* time_stamp */ '2026-10-23T22:28:14+06:00',
/* author */ (''),
/* organization */ (''),
/* preprocessor_version */ 'ST-DEVELOPER v20.2',
/* originating_system */ 'Autodesk Translation Framework v15.15.0.0',
/* authorisation */ '');

FILE_SCHEMA (('AUTOMOTIVE_DESIGN { 1 0 10303 214 3 1 1 }'));
ENDSEC;

DATA;
#10=MECHANICAL_DESIGN_GEOMETRIC_PRESENTATION_REPRESENTATION('',(#113),#6753);
#87=SHAPE_REPRESENTATION_RELATIONSHIP('SRR','None',#6810,#100);
#100=ADVANCED_BREP_SHAPE_REPRESENTATION('',(#126),#6750);
#113=STYLED_ITEM('',(#6907),#126);
#126=MANIFOLD_SOLID_BREP('Blade_07',#3762);
#180=FACE_BOUND('',#783,.T.);
#181=FACE_BOUND('',#784,.T.);
#315=PLANE('',#4296);
#316=PLANE('',#4297);
#317=PLANE('',#4298);
#318=PLANE('',#4305);
#319=PLANE('',#4308);
#320=PLANE('',#4313);
#516=FACE_OUTER_BOUND('',#780,.T.);
#517=FACE_OUTER_BOUND('',#781,.T.);
#518=FACE_OUTER_BOUND('',#782,.T.);
#519=FACE_OUTER_BOUND('',#785,.T.);
#520=FACE_OUTER_BOUND('',#786,.T.);
#521=FACE_OUTER_BOUND('',#787,.T.);
#522=FACE_OUTER_BOUND('',#788,.T.);
#523=FACE_OUTER_BOUND('',#789,.T.);
#524=FACE_OUTER_BOUND('',#790,.T.);
#525=FACE_OUTER_BOUND('',#791,.T.);
#780=EDGE_LOOP('',(#3370,#3371,#3372,#3373));
#781=EDGE_LOOP('',(#3374,#3375,#3376,#3377));
#782=EDGE_LOOP('',(#3378,#3379,#3380,#3381));
#783=EDGE_LOOP('',(#3382));
#784=EDGE_LOOP('',(#3383));
#785=EDGE_LOOP('',(#3384,#3385,#3386,#3387));
#786=EDGE_LOOP('',(#3388));
#787=EDGE_LOOP('',(#3389,#3390,#3391,#3392));
#788=EDGE_LOOP('',(#3393));
#789=EDGE_LOOP('',(#3394,#3395,#3396,#3397));
#790=EDGE_LOOP('',(#3398,#3399,#3400,#3401));
#791=EDGE_LOOP('',(#3402,#3403,#3404,#3405));
#1008=CIRCLE('',#4299,33.8);
#1009=CIRCLE('',#4300,4.99999999999999);
#1010=CIRCLE('',#4301,1.1);
#1011=CIRCLE('',#4302,1.1);
#1012=CIRCLE('',#4304,1.1);
#1013=CIRCLE('',#4307,1.1);
#1014=CIRCLE('',#4310,4.99999999999999);
#1015=CIRCLE('',#4312,33.8);
#1288=LINE('',#6592,#1574);
#1289=LINE('',#6594,#1575);
#1290=LINE('',#6596,#1576);
#1291=LINE('',#6597,#1577);
#1292=LINE('',#6601,#1578);
#1293=LINE('',#6603,#1579);
#1294=LINE('',#6605,#1580);
#1295=LINE('',#6606,#1581);
#1296=LINE('',#6617,#1582);
#1297=LINE('',#6622,#1583);
#1574=VECTOR('',#5397,10.);
#1575=VECTOR('',#5398,10.);
#1576=VECTOR('',#5399,10.);
#1577=VECTOR('',#5400,10.);
#1578=VECTOR('',#5403,10.);
#1579=VECTOR('',#5404,10.);
#1580=VECTOR('',#5405,10.);
#1581=VECTOR('',#5406,10.);
#1582=VECTOR('',#5421,1.1);
#1583=VECTOR('',#5428,1.1);
#1909=VERTEX_POINT('',#6590);
#1910=VERTEX_POINT('',#6591);
#1911=VERTEX_POINT('',#6593);
#1912=VERTEX_POINT('',#6595);
#1913=VERTEX_POINT('',#6599);
#1914=VERTEX_POINT('',#6600);
#1915=VERTEX_POINT('',#6602);
#1916=VERTEX_POINT('',#6604);
#1917=VERTEX_POINT('',#6610);
#1918=VERTEX_POINT('',#6612);
#1919=VERTEX_POINT('',#6615);
#1920=VERTEX_POINT('',#6620);
#2402=EDGE_CURVE('',#1909,#1910,#1288,.T.);
#2403=EDGE_CURVE('',#1911,#1909,#1289,.T.);
#2404=EDGE_CURVE('',#1912,#1911,#1290,.T.);
#2405=EDGE_CURVE('',#1910,#1912,#1291,.T.);
#2406=EDGE_CURVE('',#1913,#1914,#1292,.T.);
#2407=EDGE_CURVE('',#1915,#1913,#1293,.T.);
#2408=EDGE_CURVE('',#1916,#1915,#1294,.T.);
#2409=EDGE_CURVE('',#1914,#1916,#1295,.T.);
#2410=EDGE_CURVE('',#1913,#1910,#1008,.T.);
#2411=EDGE_CURVE('',#1909,#1914,#1009,.T.);
#2412=EDGE_CURVE('',#1917,#1917,#1010,.T.);
#2413=EDGE_CURVE('',#1918,#1918,#1011,.T.);
#2414=EDGE_CURVE('',#1919,#1919,#1012,.T.);
#2415=EDGE_CURVE('',#1919,#1917,#1296,.T.);
#2416=EDGE_CURVE('',#1920,#1920,#1013,.T.);
#2417=EDGE_CURVE('',#1920,#1918,#1297,.T.);
#2418=EDGE_CURVE('',#1911,#1916,#1014,.T.);
#2419=EDGE_CURVE('',#1915,#1912,#1015,.T.);
#3370=ORIENTED_EDGE('',*,*,#2402,.F.);
#3371=ORIENTED_EDGE('',*,*,#2403,.F.);
#3372=ORIENTED_EDGE('',*,*,#2404,.F.);
#3373=ORIENTED_EDGE('',*,*,#2405,.F.);
#3374=ORIENTED_EDGE('',*,*,#2406,.F.);
#3375=ORIENTED_EDGE('',*,*,#2407,.F.);
#3376=ORIENTED_EDGE('',*,*,#2408,.F.);
#3377=ORIENTED_EDGE('',*,*,#2409,.F.);
#3378=ORIENTED_EDGE('',*,*,#2402,.T.);
#3379=ORIENTED_EDGE('',*,*,#2410,.F.);
#3380=ORIENTED_EDGE('',*,*,#2406,.T.);
#3381=ORIENTED_EDGE('',*,*,#2411,.F.);
#3382=ORIENTED_EDGE('',*,*,#2412,.T.);
#3383=ORIENTED_EDGE('',*,*,#2413,.T.);
#3384=ORIENTED_EDGE('',*,*,#2414,.F.);
#3385=ORIENTED_EDGE('',*,*,#2415,.T.);
#3386=ORIENTED_EDGE('',*,*,#2412,.F.);
#3387=ORIENTED_EDGE('',*,*,#2415,.F.);
#3388=ORIENTED_EDGE('',*,*,#2414,.T.);
#3389=ORIENTED_EDGE('',*,*,#2416,.F.);
#3390=ORIENTED_EDGE('',*,*,#2417,.T.);
#3391=ORIENTED_EDGE('',*,*,#2413,.F.);
#3392=ORIENTED_EDGE('',*,*,#2417,.F.);
#3393=ORIENTED_EDGE('',*,*,#2416,.T.);
#3394=ORIENTED_EDGE('',*,*,#2403,.T.);
#3395=ORIENTED_EDGE('',*,*,#2411,.T.);
#3396=ORIENTED_EDGE('',*,*,#2409,.T.);
#3397=ORIENTED_EDGE('',*,*,#2418,.F.);
#3398=ORIENTED_EDGE('',*,*,#2405,.T.);
#3399=ORIENTED_EDGE('',*,*,#2419,.F.);
#3400=ORIENTED_EDGE('',*,*,#2407,.T.);
#3401=ORIENTED_EDGE('',*,*,#2410,.T.);
#3402=ORIENTED_EDGE('',*,*,#2404,.T.);
#3403=ORIENTED_EDGE('',*,*,#2418,.T.);
#3404=ORIENTED_EDGE('',*,*,#2408,.T.);
#3405=ORIENTED_EDGE('',*,*,#2419,.T.);
#3527=CYLINDRICAL_SURFACE('',#4303,1.1);
#3528=CYLINDRICAL_SURFACE('',#4306,1.1);
#3529=CYLINDRICAL_SURFACE('',#4309,4.99999999999999);
#3530=CYLINDRICAL_SURFACE('',#4311,33.8);
#3722=ADVANCED_FACE('',(#516),#315,.F.);
#3723=ADVANCED_FACE('',(#517),#316,.F.);
#3724=ADVANCED_FACE('',(#518,#180,#181),#317,.F.);
#3725=ADVANCED_FACE('',(#519),#3527,.T.);
#3726=ADVANCED_FACE('',(#520),#318,.F.);
#3727=ADVANCED_FACE('',(#521),#3528,.T.);
#3728=ADVANCED_FACE('',(#522),#319,.F.);
#3729=ADVANCED_FACE('',(#523),#3529,.F.);
#3730=ADVANCED_FACE('',(#524),#3530,.T.);
#3731=ADVANCED_FACE('',(#525),#320,.T.);
#3762=CLOSED_SHELL('',(#3722,#3723,#3724,#3725,#3726,#3727,#3728,#3729,
#3730,#3731));
#4295=AXIS2_PLACEMENT_3D('',#6588,#5393,#5394);
#4296=AXIS2_PLACEMENT_3D('',#6589,#5395,#5396);
#4297=AXIS2_PLACEMENT_3D('',#6598,#5401,#5402);
#4298=AXIS2_PLACEMENT_3D('',#6607,#5407,#5408);
#4299=AXIS2_PLACEMENT_3D('',#6608,#5409,#5410);
#4300=AXIS2_PLACEMENT_3D('',#6609,#5411,#5412);
#4301=AXIS2_PLACEMENT_3D('',#6611,#5413,#5414);
#4302=AXIS2_PLACEMENT_3D('',#6613,#5415,#5416);
#4303=AXIS2_PLACEMENT_3D('',#6614,#5417,#5418);
#4304=AXIS2_PLACEMENT_3D('',#6616,#5419,#5420);
#4305=AXIS2_PLACEMENT_3D('',#6618,#5422,#5423);
#4306=AXIS2_PLACEMENT_3D('',#6619,#5424,#5425);
#4307=AXIS2_PLACEMENT_3D('',#6621,#5426,#5427);
#4308=AXIS2_PLACEMENT_3D('',#6623,#5429,#5430);
#4309=AXIS2_PLACEMENT_3D('',#6624,#5431,#5432);
#4310=AXIS2_PLACEMENT_3D('',#6625,#5433,#5434);
#4311=AXIS2_PLACEMENT_3D('',#6626,#5435,#5436);
#4312=AXIS2_PLACEMENT_3D('',#6627,#5437,#5438);
#4313=AXIS2_PLACEMENT_3D('',#6628,#5439,#5440);
#5393=DIRECTION('axis',(0.,0.,1.));
#5394=DIRECTION('refdir',(1.,0.,0.));
#5395=DIRECTION('center_axis',(0.707106781186548,0.,0.707106781186547));
#5396=DIRECTION('ref_axis',(0.707106781186547,0.,-0.707106781186548));
#5397=DIRECTION('',(0.707106781186547,0.,-0.707106781186548));
#5398=DIRECTION('',(0.,-1.,0.));
#5399=DIRECTION('',(-0.707106781186547,0.,0.707106781186548));
#5400=DIRECTION('',(0.,1.,0.));
#5401=DIRECTION('center_axis',(-1.83697019872103E-16,0.,-1.));
#5402=DIRECTION('ref_axis',(-1.,0.,1.83697019872103E-16));
#5403=DIRECTION('',(-1.,0.,1.83697019872103E-16));
#5404=DIRECTION('',(0.,-1.,0.));
#5405=DIRECTION('',(1.,0.,-1.83697019872103E-16));
#5406=DIRECTION('',(0.,1.,0.));
#5407=DIRECTION('center_axis',(0.,1.,0.));
#5408=DIRECTION('ref_axis',(-1.83697019872103E-16,0.,-1.));
#5409=DIRECTION('center_axis',(0.,1.,0.));
#5410=DIRECTION('ref_axis',(-1.83697019872103E-16,0.,-1.));
#5411=DIRECTION('center_axis',(0.,-1.,0.));
#5412=DIRECTION('ref_axis',(-1.83697019872103E-16,0.,-1.));
#5413=DIRECTION('center_axis',(0.,1.,0.));
#5414=DIRECTION('ref_axis',(-1.83697019872103E-16,0.,-1.));
#5415=DIRECTION('center_axis',(0.,1.,0.));
#5416=DIRECTION('ref_axis',(-1.83697019872103E-16,0.,-1.));
#5417=DIRECTION('center_axis',(0.,-1.,0.));
#5418=DIRECTION('ref_axis',(-1.83697019872103E-16,0.,-1.));
#5419=DIRECTION('center_axis',(0.,-1.,0.));
#5420=DIRECTION('ref_axis',(-1.83697019872103E-16,0.,-1.));
#5421=DIRECTION('',(0.,1.,0.));
#5422=DIRECTION('center_axis',(0.,1.,0.));
#5423=DIRECTION('ref_axis',(-1.83697019872103E-16,0.,-1.));
#5424=DIRECTION('center_axis',(0.,-1.,0.));
#5425=DIRECTION('ref_axis',(-1.83697019872103E-16,0.,-1.));
#5426=DIRECTION('center_axis',(0.,-1.,0.));
#5427=DIRECTION('ref_axis',(-1.83697019872103E-16,0.,-1.));
#5428=DIRECTION('',(0.,1.,0.));
#5429=DIRECTION('center_axis',(0.,1.,0.));
#5430=DIRECTION('ref_axis',(-1.83697019872103E-16,0.,-1.));
#5431=DIRECTION('center_axis',(0.,1.,0.));
#5432=DIRECTION('ref_axis',(-1.83697019872103E-16,0.,-1.));
#5433=DIRECTION('center_axis',(0.,-1.,0.));
#5434=DIRECTION('ref_axis',(-1.83697019872103E-16,0.,-1.));
#5435=DIRECTION('center_axis',(0.,1.,0.));
#5436=DIRECTION('ref_axis',(-1.83697019872103E-16,0.,-1.));
#5437=DIRECTION('center_axis',(0.,1.,0.));
#5438=DIRECTION('ref_axis',(-1.83697019872103E-16,0.,-1.));
#5439=DIRECTION('center_axis',(0.,1.,0.));
#5440=DIRECTION('ref_axis',(-1.83697019872103E-16,0.,-1.));
#6588=CARTESIAN_POINT('',(0.,0.,0.));
#6589=CARTESIAN_POINT('Origin',(3.53553390593273,-3.,110.796874251098));
#6590=CARTESIAN_POINT('',(3.53553390593273,-3.,110.796874251098));
#6591=CARTESIAN_POINT('',(23.9002092041053,-3.,90.4321989529251));
#6592=CARTESIAN_POINT('',(1.76776695296637,-3.,112.564641204064));
#6593=CARTESIAN_POINT('',(3.53553390593273,-2.9,110.796874251098));
#6594=CARTESIAN_POINT('',(3.53553390593273,-3.,110.796874251098));
#6595=CARTESIAN_POINT('',(23.9002092041053,-2.9,90.4321989529251));
#6596=CARTESIAN_POINT('',(1.76776695296637,-2.9,112.564641204064));
#6597=CARTESIAN_POINT('',(23.9002092041053,-3.,90.4321989529251));
#6598=CARTESIAN_POINT('Origin',(33.8,-3.,114.33240815703));
#6599=CARTESIAN_POINT('',(33.8,-3.,114.33240815703));
#6600=CARTESIAN_POINT('',(5.,-3.,114.33240815703));
#6601=CARTESIAN_POINT('',(16.9,-3.,114.33240815703));
#6602=CARTESIAN_POINT('',(33.8,-2.9,114.33240815703));
#6603=CARTESIAN_POINT('',(33.8,-3.,114.33240815703));
#6604=CARTESIAN_POINT('',(5.,-2.9,114.33240815703));
#6605=CARTESIAN_POINT('',(16.9,-2.9,114.33240815703));
#6606=CARTESIAN_POINT('',(5.,-3.,114.33240815703));
#6607=CARTESIAN_POINT('Origin',(0.,-3.,114.33240815703));
#6608=CARTESIAN_POINT('Origin',(0.,-3.,114.33240815703));
#6609=CARTESIAN_POINT('Origin',(0.,-3.,114.33240815703));
#6610=CARTESIAN_POINT('',(28.5450224208979,-3.,109.12799088316));
#6611=CARTESIAN_POINT('Origin',(28.5450224208979,-3.,108.02799088316));
#6612=CARTESIAN_POINT('',(23.9595659283167,-3.,98.684178916323));
#6613=CARTESIAN_POINT('Origin',(23.9595659283167,-3.,97.584178916323));
#6614=CARTESIAN_POINT('Origin',(28.5450224208979,-3.,108.02799088316));
#6615=CARTESIAN_POINT('',(28.5450224208979,-3.5,109.12799088316));
#6616=CARTESIAN_POINT('Origin',(28.5450224208979,-3.5,108.02799088316));
#6617=CARTESIAN_POINT('',(28.5450224208979,-3.,109.12799088316));
#6618=CARTESIAN_POINT('Origin',(28.5450224208979,-3.5,108.02799088316));
#6619=CARTESIAN_POINT('Origin',(23.9595659283167,-3.,97.584178916323));
#6620=CARTESIAN_POINT('',(23.9595659283167,-3.5,98.684178916323));
#6621=CARTESIAN_POINT('Origin',(23.9595659283167,-3.5,97.584178916323));
#6622=CARTESIAN_POINT('',(23.9595659283167,-3.,98.684178916323));
#6623=CARTESIAN_POINT('Origin',(23.9595659283167,-3.5,97.584178916323));
#6624=CARTESIAN_POINT('Origin',(0.,-3.,114.33240815703));
#6625=CARTESIAN_POINT('Origin',(0.,-2.9,114.33240815703));
#6626=CARTESIAN_POINT('Origin',(0.,-3.,114.33240815703));
#6627=CARTESIAN_POINT('Origin',(0.,-2.9,114.33240815703));
#6628=CARTESIAN_POINT('Origin',(0.,-2.9,114.33240815703));
#6735=UNCERTAINTY_MEASURE_WITH_UNIT(LENGTH_MEASURE(0.01),#6754,
'DISTANCE_ACCURACY_VALUE',
'Maximum model space distance between geometric entities at asserted c
onnectivities');
#6738=UNCERTAINTY_MEASURE_WITH_UNIT(LENGTH_MEASURE(0.01),#6754,
'DISTANCE_ACCURACY_VALUE',
'Maximum model space distance between geometric entities at asserted c
onnectivities');
#6750=(
GEOMETRIC_REPRESENTATION_CONTEXT(3)
GLOBAL_UNCERTAINTY_ASSIGNED_CONTEXT((#6735))
GLOBAL_UNIT_ASSIGNED_CONTEXT((#6754,#6756,#6757))
REPRESENTATION_CONTEXT('','3D')
);
#6753=(
GEOMETRIC_REPRESENTATION_CONTEXT(3)
GLOBAL_UNCERTAINTY_ASSIGNED_CONTEXT((#6738))
GLOBAL_UNIT_ASSIGNED_CONTEXT((#6754,#6756,#6757))
REPRESENTATION_CONTEXT('','3D')
);
#6754=(
LENGTH_UNIT()
NAMED_UNIT(*)
SI_UNIT(.MILLI.,.METRE.)
);
#6756=(
NAMED_UNIT(*)
PLANE_ANGLE_UNIT()
SI_UNIT($,.RADIAN.)
);
#6757=(
NAMED_UNIT(*)
SI_UNIT($,.STERADIAN.)
SOLID_ANGLE_UNIT()
);
#6769=SHAPE_DEFINITION_REPRESENTATION(#6783,#6810);
#6783=PRODUCT_DEFINITION_SHAPE('',$,#6825);
#6810=SHAPE_REPRESENTATION('',(#4295),#6750);
#6813=PRODUCT_DEFINITION_CONTEXT('part definition',#6857,'design');
#6825=PRODUCT_DEFINITION('Blade_07','Blade_07',#6839,#6813);
#6839=PRODUCT_DEFINITION_FORMATION('',$,#6870);
#6857=APPLICATION_CONTEXT(
'Core Data for Automotive Mechanical Design Process');
#6858=PRODUCT_CONTEXT('part definition',#6857,'mechanical');
#6870=PRODUCT('Blade_07','Blade_07',$,(#6858));
#6901=COLOUR_RGB('Light Blue',0.38,0.62,0.78);
#6902=FILL_AREA_STYLE_COLOUR('',#6901);
#6903=FILL_AREA_STYLE('',(#6902));
#6904=SURFACE_STYLE_FILL_AREA(#6903);
#6905=SURFACE_SIDE_STYLE('',(#6904));
#6906=SURFACE_STYLE_USAGE(.BOTH.,#6905);
#6907=PRESENTATION_STYLE_ASSIGNMENT((#6906));
ENDSEC;
END-ISO-10303-21;
